ISO-10303-21;
HEADER;
/* Generated by software containing ST-Developer
 * from STEP Tools, Inc. (www.steptools.com) 
 */

FILE_DESCRIPTION(
/* description */ ('Low-profile wedge edge clamp'),
/* implementation_level */ '2;1');

FILE_NAME(
/* name */ 'Hex Bolt - M8x40.step',
/* time_stamp */ '2026-10-29T15:58:13-07:00',
/* author */ (''),
/* organization */ (''),
/* preprocessor_version */ 'ST-DEVELOPER v20.2',
/* originating_system */ 'Autodesk Translation Framework v15.17.0.0',
/* authorisation */ '');

FILE_SCHEMA (('AUTOMOTIVE_DESIGN { 1 0 10303 214 3 1 1 }'));
ENDSEC;

DATA;
#10=MECHANICAL_DESIGN_GEOMETRIC_PRESENTATION_REPRESENTATION('',(#84),#2996);
#51=(
BOUNDED_CURVE()
B_SPLINE_CURVE(2,(#2921,#2922,#2923),.UNSPECIFIED.,.F.,.F.)
B_SPLINE_CURVE_WITH_KNOTS((3,3),(0.14973948338295,0.97160236658079),
 .UNSPECIFIED.)
CURVE()
GEOMETRIC_REPRESENTATION_ITEM()
RATIONAL_B_SPLINE_CURVE((1.07140024848292,1.23714644374248,1.07140024848292))
REPRESENTATION_ITEM('')
);
#52=(
BOUNDED_CURVE()
B_SPLINE_CURVE(2,(#2925,#2926,#2927),.UNSPECIFIED.,.F.,.F.)
B_SPLINE_CURVE_WITH_KNOTS((3,3),(0.14973948338295,0.97160236658079),
 .UNSPECIFIED.)
CURVE()
GEOMETRIC_REPRESENTATION_ITEM()
RATIONAL_B_SPLINE_CURVE((1.07140024848292,1.23714644374248,1.07140024848292))
REPRESENTATION_ITEM('')
);
#53=(
BOUNDED_CURVE()
B_SPLINE_CURVE(2,(#2929,#2930,#2931),.UNSPECIFIED.,.F.,.F.)
B_SPLINE_CURVE_WITH_KNOTS((3,3),(0.14973948338295,0.97160236658079),
 .UNSPECIFIED.)
CURVE()
GEOMETRIC_REPRESENTATION_ITEM()
RATIONAL_B_SPLINE_CURVE((1.07140024848292,1.23714644374248,1.07140024848292))
REPRESENTATION_ITEM('')
);
#54=(
BOUNDED_CURVE()
B_SPLINE_CURVE(2,(#2933,#2934,#2935),.UNSPECIFIED.,.F.,.F.)
B_SPLINE_CURVE_WITH_KNOTS((3,3),(0.149739483382949,0.971602366580789),
 .UNSPECIFIED.)
CURVE()
GEOMETRIC_REPRESENTATION_ITEM()
RATIONAL_B_SPLINE_CURVE((1.07140024848292,1.23714644374248,1.07140024848292))
REPRESENTATION_ITEM('')
);
#55=(
BOUNDED_CURVE()
B_SPLINE_CURVE(2,(#2937,#2938,#2939),.UNSPECIFIED.,.F.,.F.)
B_SPLINE_CURVE_WITH_KNOTS((3,3),(0.14973948338295,0.971602366580789),
 .UNSPECIFIED.)
CURVE()
GEOMETRIC_REPRESENTATION_ITEM()
RATIONAL_B_SPLINE_CURVE((1.07140024848292,1.23714644374248,1.07140024848292))
REPRESENTATION_ITEM('')
);
#56=(
BOUNDED_CURVE()
B_SPLINE_CURVE(2,(#2940,#2941,#2942),.UNSPECIFIED.,.F.,.F.)
B_SPLINE_CURVE_WITH_KNOTS((3,3),(0.14973948338295,0.97160236658079),
 .UNSPECIFIED.)
CURVE()
GEOMETRIC_REPRESENTATION_ITEM()
RATIONAL_B_SPLINE_CURVE((1.07140024848292,1.23714644374248,1.07140024848292))
REPRESENTATION_ITEM('')
);
#60=CONICAL_SURFACE('',#1959,0.36,0.785398163397451);
#61=CONICAL_SURFACE('',#1962,0.734027674973257,1.0471975511966);
#72=SHAPE_REPRESENTATION_RELATIONSHIP('SRR','None',#3034,#78);
#78=ADVANCED_BREP_SHAPE_REPRESENTATION('',(#89),#2995);
#84=STYLED_ITEM('',(#3133),#89);
#89=MANIFOLD_SOLID_BREP('Body1',#1714);
#161=FACE_BOUND('',#465,.T.);
#199=PLANE('',#1961);
#200=PLANE('',#1964);
#201=PLANE('',#1965);
#202=PLANE('',#1966);
#203=PLANE('',#1967);
#204=PLANE('',#1968);
#205=PLANE('',#1969);
#206=PLANE('',#1970);
#207=PLANE('',#1971);
#289=FACE_OUTER_BOUND('',#453,.T.);
#290=FACE_OUTER_BOUND('',#454,.T.);
#291=FACE_OUTER_BOUND('',#455,.T.);
#292=FACE_OUTER_BOUND('',#456,.T.);
#293=FACE_OUTER_BOUND('',#457,.T.);
#294=FACE_OUTER_BOUND('',#458,.T.);
#295=FACE_OUTER_BOUND('',#459,.T.);
#296=FACE_OUTER_BOUND('',#460,.T.);
#297=FACE_OUTER_BOUND('',#461,.T.);
#298=FACE_OUTER_BOUND('',#462,.T.);
#299=FACE_OUTER_BOUND('',#463,.T.);
#300=FACE_OUTER_BOUND('',#464,.T.);
#453=EDGE_LOOP('',(#1523,#1524,#1525,#1526));
#454=EDGE_LOOP('',(#1527,#1528,#1529,#1530));
#455=EDGE_LOOP('',(#1531));
#456=EDGE_LOOP('',(#1532,#1533,#1534,#1535,#1536,#1537,#1538,#1539,#1540));
#457=EDGE_LOOP('',(#1541,#1542,#1543,#1544));
#458=EDGE_LOOP('',(#1545,#1546,#1547,#1548));
#459=EDGE_LOOP('',(#1549,#1550,#1551,#1552));
#460=EDGE_LOOP('',(#1553,#1554,#1555,#1556));
#461=EDGE_LOOP('',(#1557,#1558,#1559,#1560));
#462=EDGE_LOOP('',(#1561,#1562,#1563,#1564));
#463=EDGE_LOOP('',(#1565));
#464=EDGE_LOOP('',(#1566,#1567,#1568,#1569,#1570,#1571));
#465=EDGE_LOOP('',(#1572));
#570=LINE('',#2908,#689);
#571=LINE('',#2913,#690);
#572=LINE('',#2919,#691);
#573=LINE('',#2945,#692);
#574=LINE('',#2947,#693);
#575=LINE('',#2948,#694);
#576=LINE('',#2951,#695);
#577=LINE('',#2952,#696);
#578=LINE('',#2955,#697);
#579=LINE('',#2956,#698);
#580=LINE('',#2959,#699);
#581=LINE('',#2960,#700);
#582=LINE('',#2963,#701);
#583=LINE('',#2964,#702);
#584=LINE('',#2966,#703);
#689=VECTOR('',#2438,0.4);
#690=VECTOR('',#2445,0.36);
#691=VECTOR('',#2452,0.734027674973257);
#692=VECTOR('',#2455,1.);
#693=VECTOR('',#2456,1.);
#694=VECTOR('',#2457,1.);
#695=VECTOR('',#2460,1.);
#696=VECTOR('',#2461,1.);
#697=VECTOR('',#2464,1.);
#698=VECTOR('',#2465,1.);
#699=VECTOR('',#2468,1.);
#700=VECTOR('',#2469,1.);
#701=VECTOR('',#2472,1.);
#702=VECTOR('',#2473,1.);
#703=VECTOR('',#2476,1.);
#786=CIRCLE('',#1957,0.3933);
#787=CIRCLE('',#1958,0.3933);
#788=CIRCLE('',#1960,0.32);
#789=CIRCLE('',#1963,0.6175);
#915=VERTEX_POINT('',#2905);
#916=VERTEX_POINT('',#2907);
#917=VERTEX_POINT('',#2911);
#918=VERTEX_POINT('',#2916);
#919=VERTEX_POINT('',#2918);
#920=VERTEX_POINT('',#2920);
#921=VERTEX_POINT('',#2924);
#922=VERTEX_POINT('',#2928);
#923=VERTEX_POINT('',#2932);
#924=VERTEX_POINT('',#2936);
#925=VERTEX_POINT('',#2944);
#926=VERTEX_POINT('',#2946);
#927=VERTEX_POINT('',#2950);
#928=VERTEX_POINT('',#2954);
#929=VERTEX_POINT('',#2958);
#930=VERTEX_POINT('',#2962);
#1120=EDGE_CURVE('',#915,#915,#786,.F.);
#1121=EDGE_CURVE('',#915,#916,#570,.T.);
#1122=EDGE_CURVE('',#916,#916,#787,.F.);
#1123=EDGE_CURVE('',#917,#917,#788,.T.);
#1124=EDGE_CURVE('',#917,#915,#571,.T.);
#1125=EDGE_CURVE('',#918,#918,#789,.T.);
#1126=EDGE_CURVE('',#918,#919,#572,.T.);
#1127=EDGE_CURVE('',#920,#919,#51,.T.);
#1128=EDGE_CURVE('',#921,#920,#52,.T.);
#1129=EDGE_CURVE('',#922,#921,#53,.T.);
#1130=EDGE_CURVE('',#923,#922,#54,.T.);
#1131=EDGE_CURVE('',#924,#923,#55,.T.);
#1132=EDGE_CURVE('',#919,#924,#56,.T.);
#1133=EDGE_CURVE('',#925,#923,#573,.T.);
#1134=EDGE_CURVE('',#925,#926,#574,.T.);
#1135=EDGE_CURVE('',#926,#924,#575,.T.);
#1136=EDGE_CURVE('',#927,#922,#576,.T.);
#1137=EDGE_CURVE('',#927,#925,#577,.T.);
#1138=EDGE_CURVE('',#928,#921,#578,.T.);
#1139=EDGE_CURVE('',#928,#927,#579,.T.);
#1140=EDGE_CURVE('',#929,#920,#580,.T.);
#1141=EDGE_CURVE('',#929,#928,#581,.T.);
#1142=EDGE_CURVE('',#930,#919,#582,.T.);
#1143=EDGE_CURVE('',#930,#929,#583,.T.);
#1144=EDGE_CURVE('',#926,#930,#584,.T.);
#1523=ORIENTED_EDGE('',*,*,#1120,.F.);
#1524=ORIENTED_EDGE('',*,*,#1121,.T.);
#1525=ORIENTED_EDGE('',*,*,#1122,.F.);
#1526=ORIENTED_EDGE('',*,*,#1121,.F.);
#1527=ORIENTED_EDGE('',*,*,#1123,.F.);
#1528=ORIENTED_EDGE('',*,*,#1124,.T.);
#1529=ORIENTED_EDGE('',*,*,#1120,.T.);
#1530=ORIENTED_EDGE('',*,*,#1124,.F.);
#1531=ORIENTED_EDGE('',*,*,#1123,.T.);
#1532=ORIENTED_EDGE('',*,*,#1125,.F.);
#1533=ORIENTED_EDGE('',*,*,#1126,.T.);
#1534=ORIENTED_EDGE('',*,*,#1127,.F.);
#1535=ORIENTED_EDGE('',*,*,#1128,.F.);
#1536=ORIENTED_EDGE('',*,*,#1129,.F.);
#1537=ORIENTED_EDGE('',*,*,#1130,.F.);
#1538=ORIENTED_EDGE('',*,*,#1131,.F.);
#1539=ORIENTED_EDGE('',*,*,#1132,.F.);
#1540=ORIENTED_EDGE('',*,*,#1126,.F.);
#1541=ORIENTED_EDGE('',*,*,#1131,.T.);
#1542=ORIENTED_EDGE('',*,*,#1133,.F.);
#1543=ORIENTED_EDGE('',*,*,#1134,.T.);
#1544=ORIENTED_EDGE('',*,*,#1135,.T.);
#1545=ORIENTED_EDGE('',*,*,#1130,.T.);
#1546=ORIENTED_EDGE('',*,*,#1136,.F.);
#1547=ORIENTED_EDGE('',*,*,#1137,.T.);
#1548=ORIENTED_EDGE('',*,*,#1133,.T.);
#1549=ORIENTED_EDGE('',*,*,#1129,.T.);
#1550=ORIENTED_EDGE('',*,*,#1138,.F.);
#1551=ORIENTED_EDGE('',*,*,#1139,.T.);
#1552=ORIENTED_EDGE('',*,*,#1136,.T.);
#1553=ORIENTED_EDGE('',*,*,#1128,.T.);
#1554=ORIENTED_EDGE('',*,*,#1140,.F.);
#1555=ORIENTED_EDGE('',*,*,#1141,.T.);
#1556=ORIENTED_EDGE('',*,*,#1138,.T.);
#1557=ORIENTED_EDGE('',*,*,#1127,.T.);
#1558=ORIENTED_EDGE('',*,*,#1142,.F.);
#1559=ORIENTED_EDGE('',*,*,#1143,.T.);
#1560=ORIENTED_EDGE('',*,*,#1140,.T.);
#1561=ORIENTED_EDGE('',*,*,#1132,.T.);
#1562=ORIENTED_EDGE('',*,*,#1135,.F.);
#1563=ORIENTED_EDGE('',*,*,#1144,.T.);
#1564=ORIENTED_EDGE('',*,*,#1142,.T.);
#1565=ORIENTED_EDGE('',*,*,#1125,.T.);
#1566=ORIENTED_EDGE('',*,*,#1139,.F.);
#1567=ORIENTED_EDGE('',*,*,#1141,.F.);
#1568=ORIENTED_EDGE('',*,*,#1143,.F.);
#1569=ORIENTED_EDGE('',*,*,#1144,.F.);
#1570=ORIENTED_EDGE('',*,*,#1134,.F.);
#1571=ORIENTED_EDGE('',*,*,#1137,.F.);
#1572=ORIENTED_EDGE('',*,*,#1122,.T.);
#1614=CYLINDRICAL_SURFACE('',#1956,0.3933);
#1696=ADVANCED_FACE('',(#289),#1614,.T.);
#1697=ADVANCED_FACE('',(#290),#60,.T.);
#1698=ADVANCED_FACE('',(#291),#199,.T.);
#1699=ADVANCED_FACE('',(#292),#61,.T.);
#1700=ADVANCED_FACE('',(#293),#200,.T.);
#1701=ADVANCED_FACE('',(#294),#201,.T.);
#1702=ADVANCED_FACE('',(#295),#202,.T.);
#1703=ADVANCED_FACE('',(#296),#203,.T.);
#1704=ADVANCED_FACE('',(#297),#204,.T.);
#1705=ADVANCED_FACE('',(#298),#205,.T.);
#1706=ADVANCED_FACE('',(#299),#206,.T.);
#1707=ADVANCED_FACE('',(#300,#161),#207,.F.);
#1714=CLOSED_SHELL('',(#1696,#1697,#1698,#1699,#1700,#1701,#1702,#1703,
#1704,#1705,#1706,#1707));
#1955=AXIS2_PLACEMENT_3D('',#2903,#2432,#2433);
#1956=AXIS2_PLACEMENT_3D('',#2904,#2434,#2435);
#1957=AXIS2_PLACEMENT_3D('',#2906,#2436,#2437);
#1958=AXIS2_PLACEMENT_3D('',#2909,#2439,#2440);
#1959=AXIS2_PLACEMENT_3D('',#2910,#2441,#2442);
#1960=AXIS2_PLACEMENT_3D('',#2912,#2443,#2444);
#1961=AXIS2_PLACEMENT_3D('',#2914,#2446,#2447);
#1962=AXIS2_PLACEMENT_3D('',#2915,#2448,#2449);
#1963=AXIS2_PLACEMENT_3D('',#2917,#2450,#2451);
#1964=AXIS2_PLACEMENT_3D('',#2943,#2453,#2454);
#1965=AXIS2_PLACEMENT_3D('',#2949,#2458,#2459);
#1966=AXIS2_PLACEMENT_3D('',#2953,#2462,#2463);
#1967=AXIS2_PLACEMENT_3D('',#2957,#2466,#2467);
#1968=AXIS2_PLACEMENT_3D('',#2961,#2470,#2471);
#1969=AXIS2_PLACEMENT_3D('',#2965,#2474,#2475);
#1970=AXIS2_PLACEMENT_3D('',#2967,#2477,#2478);
#1971=AXIS2_PLACEMENT_3D('',#2968,#2479,#2480);
#2432=DIRECTION('axis',(0.,0.,1.));
#2433=DIRECTION('refdir',(1.,0.,0.));
#2434=DIRECTION('center_axis',(0.,-1.,0.));
#2435=DIRECTION('ref_axis',(1.,0.,0.));
#2436=DIRECTION('center_axis',(0.,1.,0.));
#2437=DIRECTION('ref_axis',(1.,0.,0.));
#2438=DIRECTION('',(0.,1.,0.));
#2439=DIRECTION('center_axis',(0.,-1.,0.));
#2440=DIRECTION('ref_axis',(1.,0.,0.));
#2441=DIRECTION('center_axis',(0.,1.,0.));
#2442=DIRECTION('ref_axis',(1.,0.,0.));
#2443=DIRECTION('center_axis',(0.,-1.,0.));
#2444=DIRECTION('ref_axis',(1.,0.,0.));
#2445=DIRECTION('',(-0.707106781186549,0.707106781186546,-8.65956056235496E-17));
#2446=DIRECTION('center_axis',(0.,-1.,0.));
#2447=DIRECTION('ref_axis',(0.,0.,-1.));
#2448=DIRECTION('center_axis',(0.,-1.,0.));
#2449=DIRECTION('ref_axis',(1.,0.,0.));
#2450=DIRECTION('center_axis',(0.,1.,0.));
#2451=DIRECTION('ref_axis',(1.,0.,0.));
#2452=DIRECTION('',(-0.866025403784439,-0.5,-1.06057523872491E-16));
#2453=DIRECTION('center_axis',(1.4792020664489E-16,0.,-1.));
#2454=DIRECTION('ref_axis',(-1.,0.,-1.4792020664489E-16));
#2455=DIRECTION('',(0.,1.,0.));
#2456=DIRECTION('',(-1.,0.,-1.4792020664489E-16));
#2457=DIRECTION('',(0.,1.,0.));
#2458=DIRECTION('center_axis',(0.866025403784439,0.,-0.5));
#2459=DIRECTION('ref_axis',(-0.5,0.,-0.866025403784439));
#2460=DIRECTION('',(0.,1.,0.));
#2461=DIRECTION('',(-0.5,0.,-0.866025403784439));
#2462=DIRECTION('center_axis',(0.866025403784439,0.,0.5));
#2463=DIRECTION('ref_axis',(0.5,0.,-0.866025403784439));
#2464=DIRECTION('',(0.,1.,0.));
#2465=DIRECTION('',(0.5,0.,-0.866025403784439));
#2466=DIRECTION('center_axis',(-2.95840413289779E-16,0.,1.));
#2467=DIRECTION('ref_axis',(1.,0.,2.95840413289779E-16));
#2468=DIRECTION('',(0.,1.,0.));
#2469=DIRECTION('',(1.,0.,2.95840413289779E-16));
#2470=DIRECTION('center_axis',(-0.866025403784439,0.,0.5));
#2471=DIRECTION('ref_axis',(0.5,0.,0.866025403784439));
#2472=DIRECTION('',(0.,1.,0.));
#2473=DIRECTION('',(0.5,0.,0.866025403784439));
#2474=DIRECTION('center_axis',(-0.866025403784439,0.,-0.5));
#2475=DIRECTION('ref_axis',(-0.5,0.,0.866025403784439));
#2476=DIRECTION('',(-0.5,0.,0.866025403784439));
#2477=DIRECTION('center_axis',(0.,1.,0.));
#2478=DIRECTION('ref_axis',(0.,0.,1.));
#2479=DIRECTION('center_axis',(0.,1.,0.));
#2480=DIRECTION('ref_axis',(1.,0.,0.));
#2903=CARTESIAN_POINT('',(0.,0.,0.));
#2904=CARTESIAN_POINT('Origin',(0.,-1.935,0.));
#2905=CARTESIAN_POINT('',(-0.3933,-3.9267,4.81653586104654E-17));
#2906=CARTESIAN_POINT('Origin',(0.,-3.9267,0.));
#2907=CARTESIAN_POINT('',(-0.3933,0.,-4.81653586104654E-17));
#2908=CARTESIAN_POINT('',(-0.3933,-1.935,-4.81653586104654E-17));
#2909=CARTESIAN_POINT('Origin',(0.,0.,0.));
#2910=CARTESIAN_POINT('Origin',(0.,-3.96,0.));
#2911=CARTESIAN_POINT('',(-0.32,-4.,-3.91886975727153E-17));
#2912=CARTESIAN_POINT('Origin',(0.,-4.,0.));
#2913=CARTESIAN_POINT('',(-0.36,-3.96,-4.40872847693047E-17));
#2914=CARTESIAN_POINT('Origin',(0.,-4.,0.));
#2915=CARTESIAN_POINT('Origin',(0.,0.462722715486149,0.));
#2916=CARTESIAN_POINT('',(-0.6175,0.53,-7.5621939847349E-17));
#2917=CARTESIAN_POINT('Origin',(0.,0.53,0.));
#2918=CARTESIAN_POINT('',(-0.750555349946514,0.453180457891261,-9.19165206894919E-17));
#2919=CARTESIAN_POINT('',(-0.734027674973257,0.462722715486149,-8.98924642641573E-17));
#2920=CARTESIAN_POINT('',(-0.375277674973257,0.453180457891261,0.65));
#2921=CARTESIAN_POINT('Ctrl Pts',(-0.375277674973257,0.45318045789126,0.65));
#2922=CARTESIAN_POINT('Ctrl Pts',(-0.562916512459968,0.561513791224244,
0.324999999999856));
#2923=CARTESIAN_POINT('Ctrl Pts',(-0.750555349946514,0.45318045789126,-9.19165206894919E-17));
#2924=CARTESIAN_POINT('',(0.375277674973257,0.453180457891261,0.65));
#2925=CARTESIAN_POINT('Ctrl Pts',(0.375277674973257,0.453180457891261,0.65));
#2926=CARTESIAN_POINT('Ctrl Pts',(-1.66922031752392E-13,0.561513791224244,
0.65));
#2927=CARTESIAN_POINT('Ctrl Pts',(-0.375277674973257,0.45318045789126,0.65));
#2928=CARTESIAN_POINT('',(0.750555349946514,0.453180457891261,0.));
#2929=CARTESIAN_POINT('Ctrl Pts',(0.750555349946514,0.453180457891261,0.));
#2930=CARTESIAN_POINT('Ctrl Pts',(0.562916512459802,0.561513791224244,0.325000000000144));
#2931=CARTESIAN_POINT('Ctrl Pts',(0.375277674973257,0.45318045789126,0.65));
#2932=CARTESIAN_POINT('',(0.375277674973257,0.453180457891261,-0.65));
#2933=CARTESIAN_POINT('Ctrl Pts',(0.375277674973257,0.45318045789126,-0.65));
#2934=CARTESIAN_POINT('Ctrl Pts',(0.562916512459968,0.561513791224244,-0.324999999999855));
#2935=CARTESIAN_POINT('Ctrl Pts',(0.750555349946514,0.453180457891261,0.));
#2936=CARTESIAN_POINT('',(-0.375277674973257,0.45318045789126,-0.65));
#2937=CARTESIAN_POINT('Ctrl Pts',(-0.375277674973257,0.453180457891261,
-0.65));
#2938=CARTESIAN_POINT('Ctrl Pts',(1.66866520601161E-13,0.561513791224244,
-0.65));
#2939=CARTESIAN_POINT('Ctrl Pts',(0.375277674973257,0.45318045789126,-0.65));
#2940=CARTESIAN_POINT('Ctrl Pts',(-0.750555349946514,0.453180457891261,
-9.19165206894919E-17));
#2941=CARTESIAN_POINT('Ctrl Pts',(-0.562916512459802,0.561513791224244,
-0.325000000000144));
#2942=CARTESIAN_POINT('Ctrl Pts',(-0.375277674973257,0.45318045789126,-0.65));
#2943=CARTESIAN_POINT('Origin',(0.375277674973257,0.,-0.65));
#2944=CARTESIAN_POINT('',(0.375277674973257,0.,-0.65));
#2945=CARTESIAN_POINT('',(0.375277674973257,0.,-0.65));
#2946=CARTESIAN_POINT('',(-0.375277674973257,0.,-0.65));
#2947=CARTESIAN_POINT('',(0.375277674973257,0.,-0.65));
#2948=CARTESIAN_POINT('',(-0.375277674973257,0.,-0.65));
#2949=CARTESIAN_POINT('Origin',(0.750555349946514,0.,0.));
#2950=CARTESIAN_POINT('',(0.750555349946514,0.,0.));
#2951=CARTESIAN_POINT('',(0.750555349946514,0.,0.));
#2952=CARTESIAN_POINT('',(0.750555349946514,0.,0.));
#2953=CARTESIAN_POINT('Origin',(0.375277674973257,0.,0.65));
#2954=CARTESIAN_POINT('',(0.375277674973257,0.,0.65));
#2955=CARTESIAN_POINT('',(0.375277674973257,0.,0.65));
#2956=CARTESIAN_POINT('',(0.375277674973257,0.,0.65));
#2957=CARTESIAN_POINT('Origin',(-0.375277674973257,0.,0.65));
#2958=CARTESIAN_POINT('',(-0.375277674973257,0.,0.65));
#2959=CARTESIAN_POINT('',(-0.375277674973257,0.,0.65));
#2960=CARTESIAN_POINT('',(-0.375277674973257,0.,0.65));
#2961=CARTESIAN_POINT('Origin',(-0.750555349946514,0.,-9.19165206894919E-17));
#2962=CARTESIAN_POINT('',(-0.750555349946514,0.,-9.19165206894919E-17));
#2963=CARTESIAN_POINT('',(-0.750555349946514,0.,-9.19165206894919E-17));
#2964=CARTESIAN_POINT('',(-0.750555349946514,0.,-9.19165206894919E-17));
#2965=CARTESIAN_POINT('Origin',(-0.375277674973257,0.,-0.65));
#2966=CARTESIAN_POINT('',(-0.375277674973257,0.,-0.65));
#2967=CARTESIAN_POINT('Origin',(0.,0.53,-1.11022302462516E-16));
#2968=CARTESIAN_POINT('Origin',(0.,0.,-1.11022302462516E-16));
#2986=UNCERTAINTY_MEASURE_WITH_UNIT(LENGTH_MEASURE(0.001),#2997,
'DISTANCE_ACCURACY_VALUE',
'Maximum model space distance between geometric entities at asserted c
onnectivities');
#2987=UNCERTAINTY_MEASURE_WITH_UNIT(LENGTH_MEASURE(0.001),#2997,
'DISTANCE_ACCURACY_VALUE',
'Maximum model space distance between geometric entities at asserted c
onnectivities');
#2995=(
GEOMETRIC_REPRESENTATION_CONTEXT(3)
GLOBAL_UNCERTAINTY_ASSIGNED_CONTEXT((#2986))
GLOBAL_UNIT_ASSIGNED_CONTEXT((#2997,#2999,#3000))
REPRESENTATION_CONTEXT('','3D')
);
#2996=(
GEOMETRIC_REPRESENTATION_CONTEXT(3)
GLOBAL_UNCERTAINTY_ASSIGNED_CONTEXT((#2987))
GLOBAL_UNIT_ASSIGNED_CONTEXT((#2997,#2999,#3000))
REPRESENTATION_CONTEXT('','3D')
);
#2997=(
LENGTH_UNIT()
NAMED_UNIT(*)
SI_UNIT(.CENTI.,.METRE.)
);
#2999=(
NAMED_UNIT(*)
PLANE_ANGLE_UNIT()
SI_UNIT($,.RADIAN.)
);
#3000=(
NAMED_UNIT(*)
SI_UNIT($,.STERADIAN.)
SOLID_ANGLE_UNIT()
);
#3008=SHAPE_DEFINITION_REPRESENTATION(#3016,#3034);
#3016=PRODUCT_DEFINITION_SHAPE('',$,#3043);
#3034=SHAPE_REPRESENTATION('',(#1955),#2995);
#3035=PRODUCT_DEFINITION_CONTEXT('part definition',#3061,'design');
#3043=PRODUCT_DEFINITION('Hex Bolt - M8x40','Hex Bolt - M8x40',#3051,#3035);
#3051=PRODUCT_DEFINITION_FORMATION('',$,#3070);
#3061=APPLICATION_CONTEXT(
'Core Data for Automotive Mechanical Design Process');
#3062=PRODUCT_CONTEXT('part definition',#3061,'mechanical');
#3070=PRODUCT('Hex Bolt - M8x40','Hex Bolt - M8x40','Hex Bolt - M8x40',
(#3062));
#3127=COLOUR_RGB('Black',0.12,0.14,0.17);
#3128=FILL_AREA_STYLE_COLOUR('',#3127);
#3129=FILL_AREA_STYLE('',(#3128));
#3130=SURFACE_STYLE_FILL_AREA(#3129);
#3131=SURFACE_SIDE_STYLE('',(#3130));
#3132=SURFACE_STYLE_USAGE(.BOTH.,#3131);
#3133=PRESENTATION_STYLE_ASSIGNMENT((#3132));
ENDSEC;
END-ISO-10303-21;
